ISO-10303-21;
HEADER;
/* Generated by software containing ST-Developer
 * from STEP Tools, Inc. (www.steptools.com) 
 */

FILE_DESCRIPTION(
/* description */ ('Guided pneumatic stop gate'),
/* implementation_level */ '2;1');

FILE_NAME(
/* name */ 'Flat Washer - M6.step',
/* time_stamp */ '2026-10-27T21:43:45-07:00',
/* author */ (''),
/* organization */ (''),
/* preprocessor_version */ 'ST-DEVELOPER v20.2',
/* originating_system */ 'Autodesk Translation Framework v15.17.0.0',
/* authorisation */ '');

FILE_SCHEMA (('AUTOMOTIVE_DESIGN { 1 0 10303 214 3 1 1 }'));
ENDSEC;

DATA;
#10=MECHANICAL_DESIGN_GEOMETRIC_PRESENTATION_REPRESENTATION('',(#570),#14392);
#486=SHAPE_REPRESENTATION_RELATIONSHIP('SRR','None',#14623,#528);
#528=ADVANCED_BREP_SHAPE_REPRESENTATION('',(#608),#14385);
#570=STYLED_ITEM('',(#14898),#608);
#608=MANIFOLD_SOLID_BREP('Body1',#7914);
#809=FACE_BOUND('',#2217,.T.);
#810=FACE_BOUND('',#2219,.T.);
#1086=PLANE('',#9282);
#1087=PLANE('',#9283);
#1545=FACE_OUTER_BOUND('',#2214,.T.);
#1546=FACE_OUTER_BOUND('',#2215,.T.);
#1547=FACE_OUTER_BOUND('',#2216,.T.);
#1548=FACE_OUTER_BOUND('',#2218,.T.);
#2214=EDGE_LOOP('',(#7048,#7049,#7050,#7051));
#2215=EDGE_LOOP('',(#7052,#7053,#7054,#7055));
#2216=EDGE_LOOP('',(#7056));
#2217=EDGE_LOOP('',(#7057));
#2218=EDGE_LOOP('',(#7058));
#2219=EDGE_LOOP('',(#7059));
#2774=LINE('',#13997,#3319);
#2775=LINE('',#14003,#3320);
#3319=VECTOR('',#11665,0.32);
#3320=VECTOR('',#11672,0.6);
#3706=CIRCLE('',#9277,0.32);
#3707=CIRCLE('',#9278,0.32);
#3708=CIRCLE('',#9280,0.6);
#3709=CIRCLE('',#9281,0.6);
#4294=VERTEX_POINT('',#13994);
#4295=VERTEX_POINT('',#13996);
#4296=VERTEX_POINT('',#14000);
#4297=VERTEX_POINT('',#14002);
#5222=EDGE_CURVE('',#4294,#4294,#3706,.T.);
#5223=EDGE_CURVE('',#4294,#4295,#2774,.T.);
#5224=EDGE_CURVE('',#4295,#4295,#3707,.T.);
#5225=EDGE_CURVE('',#4296,#4296,#3708,.T.);
#5226=EDGE_CURVE('',#4296,#4297,#2775,.T.);
#5227=EDGE_CURVE('',#4297,#4297,#3709,.T.);
#7048=ORIENTED_EDGE('',*,*,#5222,.F.);
#7049=ORIENTED_EDGE('',*,*,#5223,.T.);
#7050=ORIENTED_EDGE('',*,*,#5224,.T.);
#7051=ORIENTED_EDGE('',*,*,#5223,.F.);
#7052=ORIENTED_EDGE('',*,*,#5225,.F.);
#7053=ORIENTED_EDGE('',*,*,#5226,.T.);
#7054=ORIENTED_EDGE('',*,*,#5227,.T.);
#7055=ORIENTED_EDGE('',*,*,#5226,.F.);
#7056=ORIENTED_EDGE('',*,*,#5225,.T.);
#7057=ORIENTED_EDGE('',*,*,#5222,.T.);
#7058=ORIENTED_EDGE('',*,*,#5227,.F.);
#7059=ORIENTED_EDGE('',*,*,#5224,.F.);
#7387=CYLINDRICAL_SURFACE('',#9276,0.32);
#7388=CYLINDRICAL_SURFACE('',#9279,0.6);
#7827=ADVANCED_FACE('',(#1545),#7387,.F.);
#7828=ADVANCED_FACE('',(#1546),#7388,.T.);
#7829=ADVANCED_FACE('',(#1547,#809),#1086,.T.);
#7830=ADVANCED_FACE('',(#1548,#810),#1087,.F.);
#7914=CLOSED_SHELL('',(#7827,#7828,#7829,#7830));
#9275=AXIS2_PLACEMENT_3D('',#13992,#11659,#11660);
#9276=AXIS2_PLACEMENT_3D('',#13993,#11661,#11662);
#9277=AXIS2_PLACEMENT_3D('',#13995,#11663,#11664);
#9278=AXIS2_PLACEMENT_3D('',#13998,#11666,#11667);
#9279=AXIS2_PLACEMENT_3D('',#13999,#11668,#11669);
#9280=AXIS2_PLACEMENT_3D('',#14001,#11670,#11671);
#9281=AXIS2_PLACEMENT_3D('',#14004,#11673,#11674);
#9282=AXIS2_PLACEMENT_3D('',#14005,#11675,#11676);
#9283=AXIS2_PLACEMENT_3D('',#14006,#11677,#11678);
#11659=DIRECTION('axis',(0.,0.,1.));
#11660=DIRECTION('refdir',(1.,0.,0.));
#11661=DIRECTION('center_axis',(0.,1.,0.));
#11662=DIRECTION('ref_axis',(1.,0.,0.));
#11663=DIRECTION('center_axis',(0.,-1.,0.));
#11664=DIRECTION('ref_axis',(1.,0.,0.));
#11665=DIRECTION('',(0.,-1.,0.));
#11666=DIRECTION('center_axis',(0.,-1.,0.));
#11667=DIRECTION('ref_axis',(1.,0.,0.));
#11668=DIRECTION('center_axis',(0.,1.,0.));
#11669=DIRECTION('ref_axis',(1.,0.,0.));
#11670=DIRECTION('center_axis',(0.,1.,0.));
#11671=DIRECTION('ref_axis',(1.,0.,0.));
#11672=DIRECTION('',(0.,-1.,0.));
#11673=DIRECTION('center_axis',(0.,1.,0.));
#11674=DIRECTION('ref_axis',(1.,0.,0.));
#11675=DIRECTION('center_axis',(0.,1.,0.));
#11676=DIRECTION('ref_axis',(1.,0.,0.));
#11677=DIRECTION('center_axis',(0.,1.,0.));
#11678=DIRECTION('ref_axis',(1.,0.,0.));
#13992=CARTESIAN_POINT('',(0.,0.,0.));
#13993=CARTESIAN_POINT('Origin',(0.,0.,0.));
#13994=CARTESIAN_POINT('',(-0.32,0.16,3.91886975727153E-17));
#13995=CARTESIAN_POINT('Origin',(0.,0.16,0.));
#13996=CARTESIAN_POINT('',(-0.32,0.,3.91886975727153E-17));
#13997=CARTESIAN_POINT('',(-0.32,0.,3.91886975727153E-17));
#13998=CARTESIAN_POINT('Origin',(0.,0.,0.));
#13999=CARTESIAN_POINT('Origin',(0.,0.,0.));
#14000=CARTESIAN_POINT('',(-0.6,0.16,7.34788079488412E-17));
#14001=CARTESIAN_POINT('Origin',(0.,0.16,0.));
#14002=CARTESIAN_POINT('',(-0.6,0.,7.34788079488412E-17));
#14003=CARTESIAN_POINT('',(-0.6,0.,7.34788079488412E-17));
#14004=CARTESIAN_POINT('Origin',(0.,0.,0.));
#14005=CARTESIAN_POINT('Origin',(0.,0.16,0.));
#14006=CARTESIAN_POINT('Origin',(0.,0.,0.));
#14337=UNCERTAINTY_MEASURE_WITH_UNIT(LENGTH_MEASURE(0.001),#14393,
'DISTANCE_ACCURACY_VALUE',
'Maximum model space distance between geometric entities at asserted c
onnectivities');
#14344=UNCERTAINTY_MEASURE_WITH_UNIT(LENGTH_MEASURE(0.001),#14393,
'DISTANCE_ACCURACY_VALUE',
'Maximum model space distance between geometric entities at asserted c
onnectivities');
#14385=(
GEOMETRIC_REPRESENTATION_CONTEXT(3)
GLOBAL_UNCERTAINTY_ASSIGNED_CONTEXT((#14337))
GLOBAL_UNIT_ASSIGNED_CONTEXT((#14393,#14395,#14396))
REPRESENTATION_CONTEXT('','3D')
);
#14392=(
GEOMETRIC_REPRESENTATION_CONTEXT(3)
GLOBAL_UNCERTAINTY_ASSIGNED_CONTEXT((#14344))
GLOBAL_UNIT_ASSIGNED_CONTEXT((#14393,#14395,#14396))
REPRESENTATION_CONTEXT('','3D')
);
#14393=(
LENGTH_UNIT()
NAMED_UNIT(*)
SI_UNIT(.CENTI.,.METRE.)
);
#14395=(
NAMED_UNIT(*)
PLANE_ANGLE_UNIT()
SI_UNIT($,.RADIAN.)
);
#14396=(
NAMED_UNIT(*)
SI_UNIT($,.STERADIAN.)
SOLID_ANGLE_UNIT()
);
#14437=SHAPE_DEFINITION_REPRESENTATION(#14556,#14623);
#14556=PRODUCT_DEFINITION_SHAPE('',$,#14671);
#14623=SHAPE_REPRESENTATION('',(#9275),#14385);
#14630=PRODUCT_DEFINITION_CONTEXT('part definition',#14773,'design');
#14671=PRODUCT_DEFINITION('Flat Washer - M6','Flat Washer - M6',#14718,
#14630);
#14718=PRODUCT_DEFINITION_FORMATION('',$,#14815);
#14773=APPLICATION_CONTEXT(
'Core Data for Automotive Mechanical Design Process');
#14774=PRODUCT_CONTEXT('part definition',#14773,'mechanical');
#14815=PRODUCT('Flat Washer - M6','Flat Washer - M6','Flat Washer - M6',
(#14774));
#14892=COLOUR_RGB('Black',0.12,0.14,0.17);
#14893=FILL_AREA_STYLE_COLOUR('',#14892);
#14894=FILL_AREA_STYLE('',(#14893));
#14895=SURFACE_STYLE_FILL_AREA(#14894);
#14896=SURFACE_SIDE_STYLE('',(#14895));
#14897=SURFACE_STYLE_USAGE(.BOTH.,#14896);
#14898=PRESENTATION_STYLE_ASSIGNMENT((#14897));
ENDSEC;
END-ISO-10303-21;
